ISO-10303-21;
HEADER;
FILE_DESCRIPTION (('STEP AP214'),
    '1' );
FILE_NAME ('Latch Shaft Screw.step',
    '2026-10-06T13:23:30',
    ( '' ),
    ( '' ),
    'SwSTEP 2.0',
    'SolidWorks 2020',
    '' );
FILE_SCHEMA (( 'AUTOMOTIVE_DESIGN' ));
ENDSEC;

DATA;
#70=VERTEX_POINT ( 'NONE', #16012 ) ;
#100=PLANE ( 'NONE',  #11800 ) ;
#147=ORIENTED_EDGE ( 'NONE', *, *, #18826, .F. ) ;
#179=PRODUCT ( 'Latch Shaft Screw', 'Latch Shaft Screw', '', ( #7074 ) ) ;
#201=FACE_BOUND ( 'NONE', #2736, .T. ) ;
#253=EDGE_LOOP ( 'NONE', ( #22438, #23060, #147, #8100 ) ) ;
#306=STYLED_ITEM ( 'NONE', ( #22127 ), #19901 ) ;
#346=DIRECTION ( 'NONE',  ( 2.257171095940000041E-12, 1.003664318210000046E-28, 1.000000000000000000 ) ) ;
#560=DIRECTION ( 'NONE',  ( 0.000000000000000000, -1.000000000000000000, 0.000000000000000000 ) ) ;
#647=( NAMED_UNIT ( * ) SI_UNIT ( $, .STERADIAN. ) SOLID_ANGLE_UNIT ( ) );
#774=( NAMED_UNIT ( * ) PLANE_ANGLE_UNIT ( ) SI_UNIT ( $, .RADIAN. ) );
#895=FILL_AREA_STYLE ('',( #4447 ) ) ;
#912=LINE ( 'NONE', #16633, #6713 ) ;
#1004=ORIENTED_EDGE ( 'NONE', *, *, #5617, .T. ) ;
#1161=DIRECTION ( 'NONE',  ( 1.000000000000000000, 0.000000000000000000, 0.000000000000000000 ) ) ;
#1187=( NAMED_UNIT ( * ) SI_UNIT ( $, .STERADIAN. ) SOLID_ANGLE_UNIT ( ) );
#1263=EDGE_CURVE ( 'NONE', #7782, #4750, #9320, .T. ) ;
#1289=EDGE_CURVE ( 'NONE', #17090, #1341, #2215, .T. ) ;
#1341=VERTEX_POINT ( 'NONE', #7667 ) ;
#1450=CIRCLE ( 'NONE', #6356, 2.500000000000000444 ) ;
#1469=AXIS2_PLACEMENT_3D ( 'NONE', #16156, #5197, #23295 ) ;
#1510=ORIENTED_EDGE ( 'NONE', *, *, #3866, .T. ) ;
#1537=FACE_OUTER_BOUND ( 'NONE', #17839, .T. ) ;
#1605=ORIENTED_EDGE ( 'NONE', *, *, #1263, .T. ) ;
#1665=ORIENTED_EDGE ( 'NONE', *, *, #21182, .F. ) ;
#1903=DIRECTION ( 'NONE',  ( 2.257171095940000041E-12, 1.003664318210000046E-28, 1.000000000000000000 ) ) ;
#1944=DIRECTION ( 'NONE',  ( 1.000000000000000000, 0.000000000000000000, -2.253752739989067373E-12 ) ) ;
#1961=ORIENTED_EDGE ( 'NONE', *, *, #19342, .T. ) ;
#2056=VECTOR ( 'NONE', #4505, 1000.000000000000000 ) ;
#2106=CARTESIAN_POINT ( 'NONE',  ( 10.00000000010000001, 37.00000000000000000, -138.5552959529999839 ) ) ;
#2215=LINE ( 'NONE', #13488, #6466 ) ;
#2275=EDGE_CURVE ( 'NONE', #13585, #13529, #13797, .T. ) ;
#2287=CARTESIAN_POINT ( 'NONE',  ( 8.500000000050000892, 37.00000000000000000, -149.5552959529999839 ) ) ;
#2331=SURFACE_STYLE_FILL_AREA ( #895 ) ;
#2495=UNCERTAINTY_MEASURE_WITH_UNIT (LENGTH_MEASURE( 1.000000000000000082E-05 ), #9901, 'distance_accuracy_value', 'NONE');
#2551=AXIS2_PLACEMENT_3D ( 'NONE', #16524, #346, #3681 ) ;
#2667=CARTESIAN_POINT ( 'NONE',  ( 8.900000000049999471, 39.46779253580000102, -149.1552959530000066 ) ) ;
#2709=ORIENTED_EDGE ( 'NONE', *, *, #18836, .T. ) ;
#2722=AXIS2_PLACEMENT_3D ( 'NONE', #3581, #6907, #3225 ) ;
#2736=EDGE_LOOP ( 'NONE', ( #3472, #17792 ) ) ;
#2834=ORIENTED_EDGE ( 'NONE', *, *, #18308, .T. ) ;
#2913=CARTESIAN_POINT ( 'NONE',  ( 8.500000000050000892, 37.00000000000000000, -146.5552959529999839 ) ) ;
#2916=PLANE ( 'NONE',  #19017 ) ;
#3032=ORIENTED_EDGE ( 'NONE', *, *, #18308, .F. ) ;
#3082=VECTOR ( 'NONE', #6468, 1000.000000000000000 ) ;
#3092=DIRECTION ( 'NONE',  ( 1.000000000000000000, 0.000000000000000000, -2.257171095940000041E-12 ) ) ;
#3189=ORIENTED_EDGE ( 'NONE', *, *, #12349, .F. ) ;
#3225=DIRECTION ( 'NONE',  ( 1.000000000000000000, 0.000000000000000000, -2.257171095940000041E-12 ) ) ;
#3280=CARTESIAN_POINT ( 'NONE',  ( 8.900000000049999471, 37.00000000000000000, -148.7552959530000010 ) ) ;
#3352=CIRCLE ( 'NONE', #21233, 2.500000000000000444 ) ;
#3409=AXIS2_PLACEMENT_3D ( 'NONE', #10447, #10798, #19875 ) ;
#3472=ORIENTED_EDGE ( 'NONE', *, *, #3866, .F. ) ;
#3507=DIRECTION ( 'NONE',  ( 1.000000000000000000, 0.000000000000000000, -2.253752739989067373E-12 ) ) ;
#3581=CARTESIAN_POINT ( 'NONE',  ( 8.500000000050000892, 37.00000000000000000, -149.5552959529999839 ) ) ;
#3634=ADVANCED_FACE ( 'NONE', ( #4989 ), #4512, .T. ) ;
#3662=EDGE_LOOP ( 'NONE', ( #16024, #12240, #17141 ) ) ;
#3681=DIRECTION ( 'NONE',  ( 1.000000000000000000, 0.000000000000000000, -2.257453483404485639E-12 ) ) ;
#3706=DIRECTION ( 'NONE',  ( 2.257171095940000041E-12, 1.003664318210000046E-28, 1.000000000000000000 ) ) ;
#3866=EDGE_CURVE ( 'NONE', #8499, #17090, #9864, .T. ) ;
#3925=SURFACE_STYLE_FILL_AREA ( #20232 ) ;
#3942=DIRECTION ( 'NONE',  ( 1.000000000000000000, 0.000000000000000000, -2.253752739989067373E-12 ) ) ;
#4055=ORIENTED_EDGE ( 'NONE', *, *, #11777, .T. ) ;
#4085=ADVANCED_FACE ( 'NONE', ( #4606 ), #11845, .T. ) ;
#4220=ORIENTED_EDGE ( 'NONE', *, *, #12349, .T. ) ;
#4447=FILL_AREA_STYLE_COLOUR ( '', #6174 ) ;
#4505=DIRECTION ( 'NONE',  ( 0.000000000000000000, -1.000000000000000000, 0.000000000000000000 ) ) ;
#4512=CYLINDRICAL_SURFACE ( 'NONE', #17100, 1.499999999999999556 ) ;
#4590=CARTESIAN_POINT ( 'NONE',  ( 0.000000000000000000, 0.000000000000000000, 0.000000000000000000 ) ) ;
#4606=FACE_OUTER_BOUND ( 'NONE', #17372, .T. ) ;
#4627=APPLICATION_CONTEXT ( 'automotive_design' ) ;
#4725=EDGE_CURVE ( 'NONE', #12052, #13585, #3352, .T. ) ;
#4750=VERTEX_POINT ( 'NONE', #20360 ) ;
#4758=ORIENTED_EDGE ( 'NONE', *, *, #9236, .F. ) ;
#4790=FACE_OUTER_BOUND ( 'NONE', #3662, .T. ) ;
#4798=CARTESIAN_POINT ( 'NONE',  ( 7.000000000050000004, 37.00000000000000000, -146.5552959529999839 ) ) ;
#4821=CIRCLE ( 'NONE', #2551, 1.499999999999999556 ) ;
#4866=FACE_OUTER_BOUND ( 'NONE', #253, .T. ) ;
#4944=AXIS2_PLACEMENT_3D ( 'NONE', #2913, #13607, #10144 ) ;
#4976=PLANE ( 'NONE',  #13287 ) ;
#4989=FACE_OUTER_BOUND ( 'NONE', #5572, .T. ) ;
#5025=AXIS2_PLACEMENT_3D ( 'NONE', #4590, #17084, #1161 ) ;
#5134=DIRECTION ( 'NONE',  ( 1.000000000000000000, 0.000000000000000000, -2.253752739989067373E-12 ) ) ;
#5189=ORIENTED_EDGE ( 'NONE', *, *, #22222, .T. ) ;
#5197=DIRECTION ( 'NONE',  ( -1.000000000000000000, -2.602084704489999637E-17, 2.257171095940000041E-12 ) ) ;
#5255=CARTESIAN_POINT ( 'NONE',  ( 8.500000000050000892, 37.00000000000000000, -149.5552959529999839 ) ) ;
#5380=EDGE_CURVE ( 'NONE', #15072, #22346, #7439, .T. ) ;
#5572=EDGE_LOOP ( 'NONE', ( #1665, #1510, #19486, #7506 ) ) ;
#5617=EDGE_CURVE ( 'NONE', #8763, #70, #18946, .T. ) ;
#5645=DIRECTION ( 'NONE',  ( 1.000000000000000000, 0.000000000000000000, -2.253752739989067373E-12 ) ) ;
#5701=CIRCLE ( 'NONE', #4944, 2.500000000000000444 ) ;
#5779=( GEOMETRIC_REPRESENTATION_CONTEXT ( 3 ) GLOBAL_UNCERTAINTY_ASSIGNED_CONTEXT ( ( #2495 ) ) GLOBAL_UNIT_ASSIGNED_CONTEXT ( ( #9901, #13480, #647 ) ) REPRESENTATION_CONTEXT ( 'NONE', 'WORKASPACE' ) );
#5891=ADVANCED_FACE ( 'NONE', ( #4790 ), #12033, .F. ) ;
#5893=DIRECTION ( 'NONE',  ( 2.257171095940000041E-12, 1.003664318210000046E-28, 1.000000000000000000 ) ) ;
#5908=ADVANCED_FACE ( 'NONE', ( #7277 ), #12626, .T. ) ;
#5990=SURFACE_SIDE_STYLE ('',( #2331 ) ) ;
#6152=SHAPE_REPRESENTATION ( 'Latch Shaft Screw', ( #5025 ), #5779 ) ;
#6174=COLOUR_RGB ( '', 0.72549020, 0.75294118, 0.79215686) ;
#6239=DIRECTION ( 'NONE',  ( 2.257305453670000045E-12, 0.000000000000000000, 1.000000000000000000 ) ) ;
#6334=DIRECTION ( 'NONE',  ( 1.000000000000000000, 0.000000000000000000, -2.253752739989067373E-12 ) ) ;
#6356=AXIS2_PLACEMENT_3D ( 'NONE', #5255, #17752, #5134 ) ;
#6409=DIRECTION ( 'NONE',  ( 2.257171095940000041E-12, 1.003664318210000046E-28, 1.000000000000000000 ) ) ;
#6456=EDGE_LOOP ( 'NONE', ( #1004, #10179, #14601, #18644 ) ) ;
#6458=DIRECTION ( 'NONE',  ( 1.000000000000000000, 0.000000000000000000, -2.253752739989067373E-12 ) ) ;
#6466=VECTOR ( 'NONE', #6239, 1000.000000000000000 ) ;
#6468=DIRECTION ( 'NONE',  ( 2.257157423930000049E-12, 0.000000000000000000, 1.000000000000000000 ) ) ;
#6521=FACE_OUTER_BOUND ( 'NONE', #14271, .T. ) ;
#6604=UNCERTAINTY_MEASURE_WITH_UNIT (LENGTH_MEASURE( 1.000000000000000082E-05 ), #13530, 'distance_accuracy_value', 'NONE');
#6706=ORIENTED_EDGE ( 'NONE', *, *, #19289, .T. ) ;
#6713=VECTOR ( 'NONE', #10915, 1000.000000000000000 ) ;
#6720=PRODUCT_DEFINITION ( 'UNKNOWN', '', #6975, #18031 ) ;
#6771=DIRECTION ( 'NONE',  ( 1.000000000000000000, 0.000000000000000000, -2.257453483404485639E-12 ) ) ;
#6816=CIRCLE ( 'NONE', #3409, 2.500000000000000444 ) ;
#6907=DIRECTION ( 'NONE',  ( 2.257171095940000041E-12, 1.003664318210000046E-28, 1.000000000000000000 ) ) ;
#6933=EDGE_CURVE ( 'NONE', #8763, #15072, #1450, .T. ) ;
#6975=PRODUCT_DEFINITION_FORMATION_WITH_SPECIFIED_SOURCE ( 'ANY', '', #179, .NOT_KNOWN. ) ;
#7003=DIRECTION ( 'NONE',  ( 1.000000000000000000, 0.000000000000000000, -2.257453483404485639E-12 ) ) ;
#7074=PRODUCT_CONTEXT ( 'NONE', #4627, 'mechanical' ) ;
#7112=CIRCLE ( 'NONE', #7859, 2.500000000000000444 ) ;
#7200=VECTOR ( 'NONE', #21154, 1000.000000000000000 ) ;
#7228=PLANE ( 'NONE',  #1469 ) ;
#7252=CARTESIAN_POINT ( 'NONE',  ( 8.500000000050000892, 37.00000000000000000, -146.5552959529999839 ) ) ;
#7277=FACE_OUTER_BOUND ( 'NONE', #21552, .T. ) ;
#7341=CARTESIAN_POINT ( 'NONE',  ( 8.500000000050000892, 37.00000000000000000, -146.5552959529999839 ) ) ;
#7439=LINE ( 'NONE', #14702, #12107 ) ;
#7506=ORIENTED_EDGE ( 'NONE', *, *, #18836, .F. ) ;
#7593=SURFACE_SIDE_STYLE ('',( #3925 ) ) ;
#7630=AXIS2_PLACEMENT_3D ( 'NONE', #8522, #12568, #19494 ) ;
#7667=CARTESIAN_POINT ( 'NONE',  ( 7.000000000070000894, 37.00000000000000000, -138.5552959529999839 ) ) ;
#7782=VERTEX_POINT ( 'NONE', #14899 ) ;
#7859=AXIS2_PLACEMENT_3D ( 'NONE', #15030, #22068, #18483 ) ;
#7938=AXIS2_PLACEMENT_3D ( 'NONE', #15733, #22993, #12154 ) ;
#7967=AXIS2_PLACEMENT_3D ( 'NONE', #8773, #1903, #7003 ) ;
#8001=ORIENTED_EDGE ( 'NONE', *, *, #14623, .T. ) ;
#8010=CLOSED_SHELL ( 'NONE', ( #5908, #13107, #22341, #11317, #3634, #4085, #8503, #5891, #12113, #16102, #20073 ) ) ;
#8081=ADVANCED_BREP_SHAPE_REPRESENTATION ( '', ( #19901, #5025 ), #5779 ) ;
#8100=ORIENTED_EDGE ( 'NONE', *, *, #15819, .F. ) ;
#8119=SURFACE_STYLE_USAGE ( .BOTH. , #5990 ) ;
#8227=FACE_OUTER_BOUND ( 'NONE', #12197, .T. ) ;
#8374=DIRECTION ( 'NONE',  ( 1.000000000000000000, 2.602084704489999637E-17, -2.257171095940000041E-12 ) ) ;
#8438=ORIENTED_EDGE ( 'NONE', *, *, #15819, .T. ) ;
#8499=VERTEX_POINT ( 'NONE', #10425 ) ;
#8503=ADVANCED_FACE ( 'NONE', ( #6521 ), #4976, .T. ) ;
#8522=CARTESIAN_POINT ( 'NONE',  ( 8.500000000070000894, 37.00000000000000000, -138.5552959529999839 ) ) ;
#8571=CIRCLE ( 'NONE', #14674, 2.500000000000000444 ) ;
#8709=ORIENTED_EDGE ( 'NONE', *, *, #2275, .F. ) ;
#8763=VERTEX_POINT ( 'NONE', #13118 ) ;
#8773=CARTESIAN_POINT ( 'NONE',  ( 8.500000000050000892, 37.00000000000000000, -146.5552959529999839 ) ) ;
#8840=DIRECTION ( 'NONE',  ( 2.257171095940000041E-12, 1.003664318210000046E-28, 1.000000000000000000 ) ) ;
#8854=VERTEX_POINT ( 'NONE', #9415 ) ;
#8875=ORIENTED_EDGE ( 'NONE', *, *, #5617, .F. ) ;
#9071=SHAPE_DEFINITION_REPRESENTATION ( #14612, #6152 ) ;
#9085=LINE ( 'NONE', #3280, #13685 ) ;
#9118=ORIENTED_EDGE ( 'NONE', *, *, #5380, .T. ) ;
#9236=EDGE_CURVE ( 'NONE', #23304, #8854, #9085, .T. ) ;
#9312=ORIENTED_EDGE ( 'NONE', *, *, #22222, .F. ) ;
#9320=LINE ( 'NONE', #20529, #14064 ) ;
#9415=CARTESIAN_POINT ( 'NONE',  ( 8.900000000049999471, 34.53220746410000430, -148.7552959530000010 ) ) ;
#9576=CARTESIAN_POINT ( 'NONE',  ( 8.100000000049998761, 37.00000000000000000, -149.5552959529999839 ) ) ;
#9864=CIRCLE ( 'NONE', #7967, 1.499999999999999556 ) ;
#9901=( LENGTH_UNIT ( ) NAMED_UNIT ( * ) SI_UNIT ( .MILLI., .METRE. ) );
#10006=CARTESIAN_POINT ( 'NONE',  ( 8.100000000049998761, 39.46779253580000102, -148.0552959529999839 ) ) ;
#10018=( LENGTH_UNIT ( ) NAMED_UNIT ( * ) SI_UNIT ( .MILLI., .METRE. ) );
#10051=CARTESIAN_POINT ( 'NONE',  ( 8.500000000060001781, 37.00000000000000000, -142.5552959529999839 ) ) ;
#10144=DIRECTION ( 'NONE',  ( 1.000000000000000000, 0.000000000000000000, -2.253752739989067373E-12 ) ) ;
#10147=DIRECTION ( 'NONE',  ( -2.257171095940000041E-12, 0.000000000000000000, -1.000000000000000000 ) ) ;
#10150=MECHANICAL_DESIGN_GEOMETRIC_PRESENTATION_REPRESENTATION('',(#306),#16631);
#10166=LINE ( 'NONE', #13761, #10969 ) ;
#10167=VECTOR ( 'NONE', #560, 1000.000000000000000 ) ;
#10179=ORIENTED_EDGE ( 'NONE', *, *, #18826, .T. ) ;
#10207=CARTESIAN_POINT ( 'NONE',  ( 8.500000000060001781, 37.00000000000000000, -142.5552959529999839 ) ) ;
#10216=AXIS2_PLACEMENT_3D ( 'NONE', #22345, #3706, #1944 ) ;
#10277=ORIENTED_EDGE ( 'NONE', *, *, #19342, .F. ) ;
#10417=CARTESIAN_POINT ( 'NONE',  ( 6.000000000050000004, 37.00000000000000000, -149.5552959529999839 ) ) ;
#10425=CARTESIAN_POINT ( 'NONE',  ( 10.00000000010000001, 37.00000000000000000, -146.5552959529999839 ) ) ;
#10447=CARTESIAN_POINT ( 'NONE',  ( 8.500000000050000892, 37.00000000000000000, -148.7552959530000010 ) ) ;
#10500=CIRCLE ( 'NONE', #13554, 1.499999999999999556 ) ;
#10678=EDGE_CURVE ( 'NONE', #22346, #19107, #5701, .T. ) ;
#10798=DIRECTION ( 'NONE',  ( 2.257171095940000041E-12, 1.003664318210000046E-28, 1.000000000000000000 ) ) ;
#10915=DIRECTION ( 'NONE',  ( 0.000000000000000000, -1.000000000000000000, 0.000000000000000000 ) ) ;
#10969=VECTOR ( 'NONE', #20663, 1000.000000000000000 ) ;
#11110=CARTESIAN_POINT ( 'NONE',  ( 8.500000000050000892, 37.00000000000000000, -146.5552959529999839 ) ) ;
#11121=DIRECTION ( 'NONE',  ( 2.257157423930000049E-12, 0.000000000000000000, 1.000000000000000000 ) ) ;
#11159=SURFACE_STYLE_USAGE ( .BOTH. , #7593 ) ;
#11317=ADVANCED_FACE ( 'NONE', ( #13856 ), #2916, .T. ) ;
#11474=AXIS2_PLACEMENT_3D ( 'NONE', #12232, #14024, #3092 ) ;
#11673=CARTESIAN_POINT ( 'NONE',  ( 8.500000000050000892, 37.00000000000000000, -148.7552959530000010 ) ) ;
#11777=EDGE_CURVE ( 'NONE', #12052, #19107, #11928, .T. ) ;
#11800=AXIS2_PLACEMENT_3D ( 'NONE', #7341, #5893, #18170 ) ;
#11845=CYLINDRICAL_SURFACE ( 'NONE', #23130, 1.499999999999999556 ) ;
#11928=LINE ( 'NONE', #21111, #3082 ) ;
#12033=PLANE ( 'NONE',  #7938 ) ;
#12052=VERTEX_POINT ( 'NONE', #12614 ) ;
#12107=VECTOR ( 'NONE', #11121, 1000.000000000000000 ) ;
#12113=ADVANCED_FACE ( 'NONE', ( #19886 ), #12256, .F. ) ;
#12154=DIRECTION ( 'NONE',  ( 1.000000000000000000, 0.000000000000000000, -2.257171095940000041E-12 ) ) ;
#12197=EDGE_LOOP ( 'NONE', ( #15461, #9118, #3189, #18520, #22963, #10277, #8438, #8875 ) ) ;
#12203=CIRCLE ( 'NONE', #15255, 2.500000000000000444 ) ;
#12232=CARTESIAN_POINT ( 'NONE',  ( 8.900000000049999471, 37.00000000000000000, -148.7552959530000010 ) ) ;
#12235=DIRECTION ( 'NONE',  ( 1.000000000000000000, 0.000000000000000000, -2.257453483404485639E-12 ) ) ;
#12240=ORIENTED_EDGE ( 'NONE', *, *, #19289, .F. ) ;
#12247=MECHANICAL_DESIGN_GEOMETRIC_PRESENTATION_REPRESENTATION('',(#13017),#13777);
#12255=ORIENTED_EDGE ( 'NONE', *, *, #21833, .T. ) ;
#12256=PLANE ( 'NONE',  #2722 ) ;
#12349=EDGE_CURVE ( 'NONE', #19107, #22346, #12203, .T. ) ;
#12413=CARTESIAN_POINT ( 'NONE',  ( 11.00000000010000001, 37.00000000000000000, -146.5552959529999839 ) ) ;
#12568=DIRECTION ( 'NONE',  ( 2.257171095940000041E-12, 1.003664318210000046E-28, 1.000000000000000000 ) ) ;
#12614=CARTESIAN_POINT ( 'NONE',  ( 11.00000000000000000, 37.00000000000000000, -149.5552959529999839 ) ) ;
#12626=CYLINDRICAL_SURFACE ( 'NONE', #10216, 2.500000000000000444 ) ;
#12777=AXIS2_PLACEMENT_3D ( 'NONE', #21835, #8840, #3507 ) ;
#12955=FILL_AREA_STYLE_COLOUR ( '', #14734 ) ;
#13017=STYLED_ITEM ( 'NONE', ( #16831 ), #8081 ) ;
#13029=DIRECTION ( 'NONE',  ( 2.258193632089999862E-12, 0.000000000000000000, 1.000000000000000000 ) ) ;
#13089=DIRECTION ( 'NONE',  ( 2.257171095940000041E-12, 1.003664318210000046E-28, 1.000000000000000000 ) ) ;
#13107=ADVANCED_FACE ( 'NONE', ( #4866 ), #22712, .F. ) ;
#13118=CARTESIAN_POINT ( 'NONE',  ( 8.100000000049998761, 39.46779253580000102, -149.5552959529999839 ) ) ;
#13226=EDGE_LOOP ( 'NONE', ( #4220, #15333 ) ) ;
#13287=AXIS2_PLACEMENT_3D ( 'NONE', #23178, #21051, #15690 ) ;
#13325=ORIENTED_EDGE ( 'NONE', *, *, #14623, .F. ) ;
#13480=( NAMED_UNIT ( * ) PLANE_ANGLE_UNIT ( ) SI_UNIT ( $, .RADIAN. ) );
#13488=CARTESIAN_POINT ( 'NONE',  ( 7.000000000060000005, 37.00000000000000000, -142.5552959529999839 ) ) ;
#13529=VERTEX_POINT ( 'NONE', #22574 ) ;
#13530=( LENGTH_UNIT ( ) NAMED_UNIT ( * ) SI_UNIT ( .MILLI., .METRE. ) );
#13554=AXIS2_PLACEMENT_3D ( 'NONE', #7252, #19753, #6771 ) ;
#13585=VERTEX_POINT ( 'NONE', #17800 ) ;
#13607=DIRECTION ( 'NONE',  ( 2.257171095940000041E-12, 1.003664318210000046E-28, 1.000000000000000000 ) ) ;
#13627=ORIENTED_EDGE ( 'NONE', *, *, #2275, .T. ) ;
#13685=VECTOR ( 'NONE', #21383, 1000.000000000000000 ) ;
#13715=DIRECTION ( 'NONE',  ( 2.257171095940000041E-12, 1.003664318210000046E-28, 1.000000000000000000 ) ) ;
#13761=CARTESIAN_POINT ( 'NONE',  ( 10.00000000010000001, 37.00000000000000000, -142.5552959529999839 ) ) ;
#13777=( GEOMETRIC_REPRESENTATION_CONTEXT ( 3 ) GLOBAL_UNCERTAINTY_ASSIGNED_CONTEXT ( ( #17788 ) ) GLOBAL_UNIT_ASSIGNED_CONTEXT ( ( #10018, #774, #15390 ) ) REPRESENTATION_CONTEXT ( 'NONE', 'WORKASPACE' ) );
#13797=LINE ( 'NONE', #21498, #2056 ) ;
#13856=FACE_OUTER_BOUND ( 'NONE', #6456, .T. ) ;
#13882=CARTESIAN_POINT ( 'NONE',  ( 8.900000000049999471, 34.53220746410000430, -149.1552959530000066 ) ) ;
#14024=DIRECTION ( 'NONE',  ( 2.257171095940000041E-12, 1.003664318210000046E-28, 1.000000000000000000 ) ) ;
#14064=VECTOR ( 'NONE', #13029, 1000.000000000000000 ) ;
#14114=CIRCLE ( 'NONE', #7630, 1.499999999999999556 ) ;
#14271=EDGE_LOOP ( 'NONE', ( #2709, #5189 ) ) ;
#14601=ORIENTED_EDGE ( 'NONE', *, *, #1263, .F. ) ;
#14612=PRODUCT_DEFINITION_SHAPE ( 'NONE', 'NONE',  #6720 ) ;
#14623=EDGE_CURVE ( 'NONE', #8854, #13529, #21034, .T. ) ;
#14674=AXIS2_PLACEMENT_3D ( 'NONE', #11673, #22530, #6334 ) ;
#14702=CARTESIAN_POINT ( 'NONE',  ( 6.000000000050000004, 37.00000000000000000, -148.0552959529999839 ) ) ;
#14734=COLOUR_RGB ( '', 0.72549020, 0.75294118, 0.79215686) ;
#14807=VECTOR ( 'NONE', #17397, 1000.000000000000000 ) ;
#14899=CARTESIAN_POINT ( 'NONE',  ( 8.100000000049998761, 34.53220746410000430, -149.5552959529999839 ) ) ;
#14947=FACE_OUTER_BOUND ( 'NONE', #13226, .T. ) ;
#15030=CARTESIAN_POINT ( 'NONE',  ( 8.500000000050000892, 37.00000000000000000, -149.5552959529999839 ) ) ;
#15072=VERTEX_POINT ( 'NONE', #10417 ) ;
#15103=VERTEX_POINT ( 'NONE', #2106 ) ;
#15255=AXIS2_PLACEMENT_3D ( 'NONE', #11110, #19937, #5645 ) ;
#15264=APPLICATION_CONTEXT ( 'automotive_design' ) ;
#15279=LINE ( 'NONE', #2667, #16988 ) ;
#15333=ORIENTED_EDGE ( 'NONE', *, *, #10678, .T. ) ;
#15390=( NAMED_UNIT ( * ) SI_UNIT ( $, .STERADIAN. ) SOLID_ANGLE_UNIT ( ) );
#15461=ORIENTED_EDGE ( 'NONE', *, *, #6933, .T. ) ;
#15498=CYLINDRICAL_SURFACE ( 'NONE', #22267, 2.500000000000000444 ) ;
#15690=DIRECTION ( 'NONE',  ( 1.000000000000000000, 0.000000000000000000, -2.257171095940000041E-12 ) ) ;
#15733=CARTESIAN_POINT ( 'NONE',  ( 8.500000000050000892, 37.00000000000000000, -149.5552959529999839 ) ) ;
#15734=EDGE_LOOP ( 'NONE', ( #8709, #23315, #3032 ) ) ;
#15819=EDGE_CURVE ( 'NONE', #23304, #70, #8571, .T. ) ;
#16012=CARTESIAN_POINT ( 'NONE',  ( 8.100000000049998761, 39.46779253580000102, -148.7552959530000010 ) ) ;
#16024=ORIENTED_EDGE ( 'NONE', *, *, #20195, .T. ) ;
#16102=ADVANCED_FACE ( 'NONE', ( #8227 ), #15498, .T. ) ;
#16156=CARTESIAN_POINT ( 'NONE',  ( 8.900000000049999471, 37.00000000000000000, -148.7552959530000010 ) ) ;
#16524=CARTESIAN_POINT ( 'NONE',  ( 8.500000000070000894, 37.00000000000000000, -138.5552959529999839 ) ) ;
#16631=( GEOMETRIC_REPRESENTATION_CONTEXT ( 3 ) GLOBAL_UNCERTAINTY_ASSIGNED_CONTEXT ( ( #6604 ) ) GLOBAL_UNIT_ASSIGNED_CONTEXT ( ( #13530, #21165, #1187 ) ) REPRESENTATION_CONTEXT ( 'NONE', 'WORKASPACE' ) );
#16633=CARTESIAN_POINT ( 'NONE',  ( 8.100000000049998761, 37.00000000000000000, -148.7552959530000010 ) ) ;
#16831=PRESENTATION_STYLE_ASSIGNMENT (( #8119 ) ) ;
#16932=DIRECTION ( 'NONE',  ( -2.258193632089999862E-12, 0.000000000000000000, -1.000000000000000000 ) ) ;
#16988=VECTOR ( 'NONE', #16932, 1000.000000000000000 ) ;
#17084=DIRECTION ( 'NONE',  ( 0.000000000000000000, 0.000000000000000000, 1.000000000000000000 ) ) ;
#17090=VERTEX_POINT ( 'NONE', #4798 ) ;
#17100=AXIS2_PLACEMENT_3D ( 'NONE', #10207, #6409, #12235 ) ;
#17141=ORIENTED_EDGE ( 'NONE', *, *, #6933, .F. ) ;
#17372=EDGE_LOOP ( 'NONE', ( #20234, #22217, #21026, #9312 ) ) ;
#17397=DIRECTION ( 'NONE',  ( 2.257157423930000049E-12, 0.000000000000000000, 1.000000000000000000 ) ) ;
#17752=DIRECTION ( 'NONE',  ( 2.257171095940000041E-12, 1.003664318210000046E-28, 1.000000000000000000 ) ) ;
#17788=UNCERTAINTY_MEASURE_WITH_UNIT (LENGTH_MEASURE( 1.000000000000000082E-05 ), #10018, 'distance_accuracy_value', 'NONE');
#17792=ORIENTED_EDGE ( 'NONE', *, *, #18782, .F. ) ;
#17800=CARTESIAN_POINT ( 'NONE',  ( 8.900000000049999471, 39.46779253580000102, -149.5552959529999839 ) ) ;
#17839=EDGE_LOOP ( 'NONE', ( #1961, #13627, #13325, #4758 ) ) ;
#18031=PRODUCT_DEFINITION_CONTEXT ( 'detailed design', #15264, 'design' ) ;
#18170=DIRECTION ( 'NONE',  ( 1.000000000000000000, 0.000000000000000000, -2.257171095940000041E-12 ) ) ;
#18308=EDGE_CURVE ( 'NONE', #13529, #12052, #19234, .T. ) ;
#18483=DIRECTION ( 'NONE',  ( 1.000000000000000000, 0.000000000000000000, -2.253752739989067373E-12 ) ) ;
#18520=ORIENTED_EDGE ( 'NONE', *, *, #11777, .F. ) ;
#18637=LINE ( 'NONE', #9576, #10167 ) ;
#18644=ORIENTED_EDGE ( 'NONE', *, *, #20195, .F. ) ;
#18782=EDGE_CURVE ( 'NONE', #17090, #8499, #10500, .T. ) ;
#18826=EDGE_CURVE ( 'NONE', #70, #4750, #912, .T. ) ;
#18836=EDGE_CURVE ( 'NONE', #15103, #1341, #4821, .T. ) ;
#18946=LINE ( 'NONE', #10006, #14807 ) ;
#19017=AXIS2_PLACEMENT_3D ( 'NONE', #21124, #8374, #10147 ) ;
#19107=VERTEX_POINT ( 'NONE', #12413 ) ;
#19229=DIRECTION ( 'NONE',  ( 2.257171095940000041E-12, 1.003664318210000046E-28, 1.000000000000000000 ) ) ;
#19234=CIRCLE ( 'NONE', #12777, 2.500000000000000444 ) ;
#19289=EDGE_CURVE ( 'NONE', #15072, #7782, #7112, .T. ) ;
#19342=EDGE_CURVE ( 'NONE', #23304, #13585, #15279, .T. ) ;
#19486=ORIENTED_EDGE ( 'NONE', *, *, #1289, .T. ) ;
#19494=DIRECTION ( 'NONE',  ( 1.000000000000000000, 0.000000000000000000, -2.257453483404485639E-12 ) ) ;
#19753=DIRECTION ( 'NONE',  ( 2.257171095940000041E-12, 1.003664318210000046E-28, 1.000000000000000000 ) ) ;
#19875=DIRECTION ( 'NONE',  ( 1.000000000000000000, 0.000000000000000000, -2.253752739989067373E-12 ) ) ;
#19886=FACE_OUTER_BOUND ( 'NONE', #15734, .T. ) ;
#19901=MANIFOLD_SOLID_BREP ( 'lock_assembly.1\\Product1.1\\Part10.1\\PartBody', #8010 ) ;
#19937=DIRECTION ( 'NONE',  ( 2.257171095940000041E-12, 1.003664318210000046E-28, 1.000000000000000000 ) ) ;
#20073=ADVANCED_FACE ( 'NONE', ( #1537 ), #7228, .T. ) ;
#20195=EDGE_CURVE ( 'NONE', #8763, #7782, #18637, .T. ) ;
#20232=FILL_AREA_STYLE ('',( #12955 ) ) ;
#20234=ORIENTED_EDGE ( 'NONE', *, *, #1289, .F. ) ;
#20289=ORIENTED_EDGE ( 'NONE', *, *, #10678, .F. ) ;
#20360=CARTESIAN_POINT ( 'NONE',  ( 8.100000000049998761, 34.53220746410000430, -148.7552959530000010 ) ) ;
#20529=CARTESIAN_POINT ( 'NONE',  ( 8.100000000049998761, 34.53220746410000430, -149.1552959530000066 ) ) ;
#20663=DIRECTION ( 'NONE',  ( 2.257305453670000045E-12, 0.000000000000000000, 1.000000000000000000 ) ) ;
#20754=SHAPE_REPRESENTATION_RELATIONSHIP ( 'NONE' , 'NONE' ,  #6152, #8081 ) ;
#21026=ORIENTED_EDGE ( 'NONE', *, *, #21182, .T. ) ;
#21034=LINE ( 'NONE', #13882, #7200 ) ;
#21051=DIRECTION ( 'NONE',  ( 2.257171095940000041E-12, 1.003664318210000046E-28, 1.000000000000000000 ) ) ;
#21111=CARTESIAN_POINT ( 'NONE',  ( 11.00000000010000001, 37.00000000000000000, -148.0552959529999839 ) ) ;
#21124=CARTESIAN_POINT ( 'NONE',  ( 8.100000000049998761, 37.00000000000000000, -149.5552959529999839 ) ) ;
#21151=DIRECTION ( 'NONE',  ( 1.000000000000000000, 0.000000000000000000, -2.257453483404485639E-12 ) ) ;
#21154=DIRECTION ( 'NONE',  ( -2.258193632089999862E-12, 0.000000000000000000, -1.000000000000000000 ) ) ;
#21165=( NAMED_UNIT ( * ) PLANE_ANGLE_UNIT ( ) SI_UNIT ( $, .RADIAN. ) );
#21182=EDGE_CURVE ( 'NONE', #8499, #15103, #10166, .T. ) ;
#21233=AXIS2_PLACEMENT_3D ( 'NONE', #2287, #13089, #3942 ) ;
#21383=DIRECTION ( 'NONE',  ( 0.000000000000000000, -1.000000000000000000, 0.000000000000000000 ) ) ;
#21498=CARTESIAN_POINT ( 'NONE',  ( 8.900000000049999471, 37.00000000000000000, -149.5552959529999839 ) ) ;
#21552=EDGE_LOOP ( 'NONE', ( #2834, #4055, #20289, #23151, #6706, #1605, #12255, #8001 ) ) ;
#21833=EDGE_CURVE ( 'NONE', #4750, #8854, #6816, .T. ) ;
#21835=CARTESIAN_POINT ( 'NONE',  ( 8.500000000050000892, 37.00000000000000000, -149.5552959529999839 ) ) ;
#21974=CARTESIAN_POINT ( 'NONE',  ( 6.000000000050000004, 37.00000000000000000, -146.5552959529999839 ) ) ;
#22068=DIRECTION ( 'NONE',  ( 2.257171095940000041E-12, 1.003664318210000046E-28, 1.000000000000000000 ) ) ;
#22127=PRESENTATION_STYLE_ASSIGNMENT (( #11159 ) ) ;
#22217=ORIENTED_EDGE ( 'NONE', *, *, #18782, .T. ) ;
#22222=EDGE_CURVE ( 'NONE', #1341, #15103, #14114, .T. ) ;
#22267=AXIS2_PLACEMENT_3D ( 'NONE', #22758, #13715, #6458 ) ;
#22341=ADVANCED_FACE ( 'NONE', ( #201, #14947 ), #100, .T. ) ;
#22345=CARTESIAN_POINT ( 'NONE',  ( 8.500000000050000892, 37.00000000000000000, -148.0552959529999839 ) ) ;
#22346=VERTEX_POINT ( 'NONE', #21974 ) ;
#22438=ORIENTED_EDGE ( 'NONE', *, *, #9236, .T. ) ;
#22530=DIRECTION ( 'NONE',  ( 2.257171095940000041E-12, 1.003664318210000046E-28, 1.000000000000000000 ) ) ;
#22574=CARTESIAN_POINT ( 'NONE',  ( 8.900000000049999471, 34.53220746410000430, -149.5552959529999839 ) ) ;
#22704=CARTESIAN_POINT ( 'NONE',  ( 8.900000000049999471, 39.46779253580000102, -148.7552959530000010 ) ) ;
#22712=PLANE ( 'NONE',  #11474 ) ;
#22758=CARTESIAN_POINT ( 'NONE',  ( 8.500000000050000892, 37.00000000000000000, -148.0552959529999839 ) ) ;
#22963=ORIENTED_EDGE ( 'NONE', *, *, #4725, .T. ) ;
#22993=DIRECTION ( 'NONE',  ( 2.257171095940000041E-12, 1.003664318210000046E-28, 1.000000000000000000 ) ) ;
#23060=ORIENTED_EDGE ( 'NONE', *, *, #21833, .F. ) ;
#23130=AXIS2_PLACEMENT_3D ( 'NONE', #10051, #19229, #21151 ) ;
#23151=ORIENTED_EDGE ( 'NONE', *, *, #5380, .F. ) ;
#23178=CARTESIAN_POINT ( 'NONE',  ( 8.500000000070000894, 37.00000000000000000, -138.5552959529999839 ) ) ;
#23295=DIRECTION ( 'NONE',  ( -2.602084704489999637E-17, 1.000000000000000000, 0.000000000000000000 ) ) ;
#23304=VERTEX_POINT ( 'NONE', #22704 ) ;
#23315=ORIENTED_EDGE ( 'NONE', *, *, #4725, .F. ) ;
ENDSEC;
END-ISO-10303-21;
